ISO-10303-21;
HEADER;
FILE_DESCRIPTION (('STEP AP214'),
    '1' );
FILE_NAME ('socket head cap screw_iso_ISO 4762 M4 x 25 - 25N.step',
    '2026-10-03T20:08:58',
    ( '' ),
    ( '' ),
    'SwSTEP 2.0',
    'SolidWorks 2026',
    '' );
FILE_SCHEMA (( 'AUTOMOTIVE_DESIGN' ));
ENDSEC;

DATA;
#1=FACE_OUTER_BOUND ( 'NONE', #4766, .T. ) ;
#56=ADVANCED_FACE ( 'NONE', ( #4070, #400 ), #9089, .T. ) ;
#79=LINE ( 'NONE', #4007, #1843 ) ;
#93=VERTEX_POINT ( 'NONE', #9152 ) ;
#96=EDGE_LOOP ( 'NONE', ( #11303, #3914, #11621, #9750 ) ) ;
#163=CARTESIAN_POINT ( 'NONE',  ( 4.000000000000003553, 1.942890293094023946E-16, 3.500000000000003997 ) ) ;
#191=ORIENTED_EDGE ( 'NONE', *, *, #10270, .T. ) ;
#192=PLANE ( 'NONE',  #6009 ) ;
#194=FACE_OUTER_BOUND ( 'NONE', #7754, .T. ) ;
#200=CARTESIAN_POINT ( 'NONE',  ( 2.000000000000001776, 0.000000000000000000, 0.000000000000000000 ) ) ;
#271=VERTEX_POINT ( 'NONE', #9524 ) ;
#281=AXIS2_PLACEMENT_3D ( 'NONE', #5557, #12328, #3506 ) ;
#300=AXIS2_PLACEMENT_3D ( 'NONE', #8481, #819, #7524 ) ;
#322=SHAPE_REPRESENTATION_RELATIONSHIP ( 'NONE' , 'NONE' ,  #4436, #9258 ) ;
#336=DIRECTION ( 'NONE',  ( -2.218671295934093250E-30, 5.551115123125776539E-17, 1.000000000000000000 ) ) ;
#341=DIRECTION ( 'NONE',  ( 0.000000000000000000, -5.551115123125770376E-17, -1.000000000000000000 ) ) ;
#342=EDGE_CURVE ( 'NONE', #10168, #10108, #1081, .T. ) ;
#378=DIRECTION ( 'NONE',  ( -1.000000000000000000, -1.031065855027150586E-29, 2.218671295934095703E-30 ) ) ;
#380=EDGE_LOOP ( 'NONE', ( #7389, #11762, #9800, #764, #11312 ) ) ;
#382=EDGE_CURVE ( 'NONE', #5244, #271, #8885, .T. ) ;
#387=AXIS2_PLACEMENT_3D ( 'NONE', #558, #4558, #8470 ) ;
#396=VECTOR ( 'NONE', #12270, 999.9999999999998863 ) ;
#400=FACE_OUTER_BOUND ( 'NONE', #10400, .T. ) ;
#474=DIRECTION ( 'NONE',  ( 1.000000000000000000, 1.031065855027150586E-29, -2.218671295934095703E-30 ) ) ;
#492=ORIENTED_EDGE ( 'NONE', *, *, #6966, .T. ) ;
#494=CIRCLE ( 'NONE', #6686, 3.500000000000003997 ) ;
#558=CARTESIAN_POINT ( 'NONE',  ( 2.000000000000001776, 1.773042676681338303, 0.000000000000000000 ) ) ;
#559=ORIENTED_EDGE ( 'NONE', *, *, #8524, .T. ) ;
#579=DIRECTION ( 'NONE',  ( -1.000000000000000000, -1.031065855027150586E-29, 2.218671295934095703E-30 ) ) ;
#622=EDGE_LOOP ( 'NONE', ( #3676, #3144, #3031 ) ) ;
#658=EDGE_CURVE ( 'NONE', #5057, #3716, #851, .T. ) ;
#764=ORIENTED_EDGE ( 'NONE', *, *, #1551, .T. ) ;
#791=ORIENTED_EDGE ( 'NONE', *, *, #10760, .F. ) ;
#800=AXIS2_PLACEMENT_3D ( 'NONE', #1062, #6025, #7952 ) ;
#810=COLOUR_RGB ( '', 0.72549020, 0.75294118, 0.79215686) ;
#819=DIRECTION ( 'NONE',  ( 1.031065855027150586E-29, -1.000000000000000000, 5.551115123125776539E-17 ) ) ;
#838=EDGE_CURVE ( 'NONE', #4187, #10144, #4093, .T. ) ;
#851=CIRCLE ( 'NONE', #2312, 3.300000000000003375 ) ;
#910=CARTESIAN_POINT ( 'NONE',  ( 2.000000000000001776, 1.773042676681338303, 0.000000000000000000 ) ) ;
#922=LINE ( 'NONE', #4918, #1295 ) ;
#928=LINE ( 'NONE', #7998, #7727 ) ;
#935=EDGE_LOOP ( 'NONE', ( #8597, #11513, #1513, #7375, #1039 ) ) ;
#960=ORIENTED_EDGE ( 'NONE', *, *, #1412, .F. ) ;
#963=FACE_OUTER_BOUND ( 'NONE', #622, .T. ) ;
#966=ADVANCED_FACE ( 'NONE', ( #11308 ), #6217, .T. ) ;
#979=ORIENTED_EDGE ( 'NONE', *, *, #6966, .F. ) ;
#980=ORIENTED_EDGE ( 'NONE', *, *, #10516, .T. ) ;
#1004=VECTOR ( 'NONE', #9771, 1000.000000000000000 ) ;
#1033=DIRECTION ( 'NONE',  ( -1.000000000000000000, -1.031065855027150586E-29, 2.218671295934095703E-30 ) ) ;
#1039=ORIENTED_EDGE ( 'NONE', *, *, #3460, .T. ) ;
#1042=PLANE ( 'NONE',  #9781 ) ;
#1052=DIRECTION ( 'NONE',  ( -7.818312609239974136E-30, -0.8660254037844390407, -0.4999999999999992784 ) ) ;
#1053=VERTEX_POINT ( 'NONE', #3220 ) ;
#1054=EDGE_LOOP ( 'NONE', ( #10463, #2615, #10847, #11911 ) ) ;
#1057=VERTEX_POINT ( 'NONE', #4225 ) ;
#1062=CARTESIAN_POINT ( 'NONE',  ( 28.61000000000001009, 3.469446951953614189E-15, 0.000000000000000000 ) ) ;
#1081=CIRCLE ( 'NONE', #2755, 1.535500000000001863 ) ;
#1090=VERTEX_POINT ( 'NONE', #1574 ) ;
#1108=DIRECTION ( 'NONE',  ( 1.031682152609352680E-29, 1.000000000000000000, -1.498801083243958569E-15 ) ) ;
#1115=LINE ( 'NONE', #8969, #5641 ) ;
#1162=AXIS2_PLACEMENT_3D ( 'NONE', #2759, #10321, #6545 ) ;
#1174=DIRECTION ( 'NONE',  ( 1.000000000000000000, 1.031065855027150586E-29, 2.218671295934092550E-30 ) ) ;
#1214=DIRECTION ( 'NONE',  ( 1.031682152609352680E-29, 1.000000000000000000, -1.498801083243958569E-15 ) ) ;
#1237=DIRECTION ( 'NONE',  ( -3.260214209858708648E-30, -0.5000000000000012212, -0.8660254037844380415 ) ) ;
#1291=CARTESIAN_POINT ( 'NONE',  ( 2.000000000000001776, -0.8865213383406727043, 1.535500000000009191 ) ) ;
#1295=VECTOR ( 'NONE', #3707, 1000.000000000000000 ) ;
#1334=ORIENTED_EDGE ( 'NONE', *, *, #10118, .F. ) ;
#1342=ORIENTED_EDGE ( 'NONE', *, *, #9256, .T. ) ;
#1343=EDGE_LOOP ( 'NONE', ( #979, #8656, #191, #6990, #9068 ) ) ;
#1373=PLANE ( 'NONE',  #10921 ) ;
#1412=EDGE_CURVE ( 'NONE', #1057, #7720, #9213, .T. ) ;
#1416=CARTESIAN_POINT ( 'NONE',  ( 3.999999999999996447, 0.000000000000000000, 0.000000000000000000 ) ) ;
#1439=DIRECTION ( 'NONE',  ( 1.000000000000000000, 1.031065855027150586E-29, 2.218671295934092550E-30 ) ) ;
#1455=MECHANICAL_DESIGN_GEOMETRIC_PRESENTATION_REPRESENTATION('',(#2072),#11342);
#1471=LINE ( 'NONE', #3610, #7618 ) ;
#1476=( NAMED_UNIT ( * ) PLANE_ANGLE_UNIT ( ) SI_UNIT ( $, .RADIAN. ) );
#1500=EDGE_CURVE ( 'NONE', #3716, #5057, #2889, .T. ) ;
#1501=CARTESIAN_POINT ( 'NONE',  ( 2.000000000000001776, 0.8865213383406657099, 1.535500000000022958 ) ) ;
#1513=ORIENTED_EDGE ( 'NONE', *, *, #8524, .F. ) ;
#1522=EDGE_CURVE ( 'NONE', #1090, #7272, #12705, .T. ) ;
#1529=EDGE_LOOP ( 'NONE', ( #9834, #5911, #8287, #3014, #1342 ) ) ;
#1540=( NAMED_UNIT ( * ) SI_UNIT ( $, .STERADIAN. ) SOLID_ANGLE_UNIT ( ) );
#1541=CIRCLE ( 'NONE', #12254, 2.000000000000003553 ) ;
#1551=EDGE_CURVE ( 'NONE', #10108, #10778, #3849, .T. ) ;
#1574=CARTESIAN_POINT ( 'NONE',  ( 28.61000000000001009, 3.580469254416129843E-15, 2.000000000000003553 ) ) ;
#1582=VERTEX_POINT ( 'NONE', #1846 ) ;
#1585=PRODUCT_DEFINITION_FORMATION_WITH_SPECIFIED_SOURCE ( 'ANY', '', #8328, .NOT_KNOWN. ) ;
#1587=CIRCLE ( 'NONE', #5906, 3.500000000000003997 ) ;
#1588=VECTOR ( 'NONE', #11611, 999.9999999999998863 ) ;
#1593=EDGE_LOOP ( 'NONE', ( #10858, #8430 ) ) ;
#1618=VERTEX_POINT ( 'NONE', #163 ) ;
#1645=CYLINDRICAL_SURFACE ( 'NONE', #11220, 3.500000000000003997 ) ;
#1647=ORIENTED_EDGE ( 'NONE', *, *, #5811, .T. ) ;
#1668=EDGE_LOOP ( 'NONE', ( #2219, #492, #3445, #8221, #7910 ) ) ;
#1676=EDGE_CURVE ( 'NONE', #10778, #4568, #11050, .T. ) ;
#1704=CARTESIAN_POINT ( 'NONE',  ( 0.1999999999999987899, 0.000000000000000000, 0.000000000000000000 ) ) ;
#1731=ORIENTED_EDGE ( 'NONE', *, *, #1522, .T. ) ;
#1759=DIRECTION ( 'NONE',  ( -1.000000000000000000, -1.031065855027150586E-29, 2.218671295934095703E-30 ) ) ;
#1760=LINE ( 'NONE', #8775, #9472 ) ;
#1764=ORIENTED_EDGE ( 'NONE', *, *, #9514, .T. ) ;
#1829=DIRECTION ( 'NONE',  ( -7.025792437124625182E-30, -0.4999999999999992784, 0.8660254037844390407 ) ) ;
#1837=ORIENTED_EDGE ( 'NONE', *, *, #11450, .F. ) ;
#1843=VECTOR ( 'NONE', #8772, 1000.000000000000000 ) ;
#1844=ORIENTED_EDGE ( 'NONE', *, *, #5034, .T. ) ;
#1846=CARTESIAN_POINT ( 'NONE',  ( 2.000000000000001776, -0.8865213383406727043, 1.535500000000009191 ) ) ;
#1882=( LENGTH_UNIT ( ) NAMED_UNIT ( * ) SI_UNIT ( .MILLI., .METRE. ) );
#1894=CYLINDRICAL_SURFACE ( 'NONE', #3820, 2.000000000000003109 ) ;
#1908=DIRECTION ( 'NONE',  ( 1.000867273499157327E-29, 0.8660254037844379305, -0.5000000000000012212 ) ) ;
#1911=DIRECTION ( 'NONE',  ( 3.260214209858707948E-30, 0.5000000000000011102, 0.8660254037844380415 ) ) ;
#1933=CARTESIAN_POINT ( 'NONE',  ( 2.000000000000001776, 0.8865213383406657099, 1.535500000000022958 ) ) ;
#1972=LINE ( 'NONE', #6944, #8795 ) ;
#1974=DIRECTION ( 'NONE',  ( 0.000000000000000000, 5.551115123125776539E-17, 1.000000000000000000 ) ) ;
#1980=VECTOR ( 'NONE', #7321, 1000.000000000000000 ) ;
#1990=PRODUCT_DEFINITION_CONTEXT ( 'detailed design', #7485, 'design' ) ;
#2002=CARTESIAN_POINT ( 'NONE',  ( 2.000000000000001776, -0.8865213383406727043, 1.535500000000009191 ) ) ;
#2017=CARTESIAN_POINT ( 'NONE',  ( 0.1999999999999987899, 0.000000000000000000, 0.000000000000000000 ) ) ;
#2018=EDGE_CURVE ( 'NONE', #93, #11435, #10677, .T. ) ;
#2058=ORIENTED_EDGE ( 'NONE', *, *, #1412, .T. ) ;
#2072=STYLED_ITEM ( 'NONE', ( #10216 ), #9258 ) ;
#2079=COLOUR_RGB ( '', 0.72549020, 0.75294118, 0.79215686) ;
#2101=DIRECTION ( 'NONE',  ( -1.000000000000000000, -1.031065855027150586E-29, 2.218671295934095703E-30 ) ) ;
#2177=ORIENTED_EDGE ( 'NONE', *, *, #8399, .F. ) ;
#2195=ORIENTED_EDGE ( 'NONE', *, *, #10516, .F. ) ;
#2204=VECTOR ( 'NONE', #1108, 1000.000000000000000 ) ;
#2219=ORIENTED_EDGE ( 'NONE', *, *, #9775, .F. ) ;
#2231=CARTESIAN_POINT ( 'NONE',  ( 28.99999999999999645, 3.469446951953614189E-15, 0.000000000000000000 ) ) ;
#2256=AXIS2_PLACEMENT_3D ( 'NONE', #3479, #11264, #10340 ) ;
#2273=FACE_OUTER_BOUND ( 'NONE', #1529, .T. ) ;
#2277=AXIS2_PLACEMENT_3D ( 'NONE', #9966, #11016, #8044 ) ;
#2283=LINE ( 'NONE', #11880, #2343 ) ;
#2291=CARTESIAN_POINT ( 'NONE',  ( 2.000000000000001776, -1.329782007511007169, -0.7677499999999976010 ) ) ;
#2301=EDGE_CURVE ( 'NONE', #10144, #7729, #4839, .T. ) ;
#2304=CARTESIAN_POINT ( 'NONE',  ( -31.74999999999995026, 0.000000000000000000, 6.938893903907228378E-15 ) ) ;
#2307=AXIS2_PLACEMENT_3D ( 'NONE', #8456, #9535, #3641 ) ;
#2312=AXIS2_PLACEMENT_3D ( 'NONE', #3373, #579, #7475 ) ;
#2334=EDGE_CURVE ( 'NONE', #271, #7997, #9244, .T. ) ;
#2343=VECTOR ( 'NONE', #1237, 999.9999999999998863 ) ;
#2358=ORIENTED_EDGE ( 'NONE', *, *, #7362, .T. ) ;
#2383=ORIENTED_EDGE ( 'NONE', *, *, #382, .T. ) ;
#2403=ADVANCED_FACE ( 'NONE', ( #194 ), #6185, .T. ) ;
#2433=DIRECTION ( 'NONE',  ( -1.000000000000000000, -1.031065855027150586E-29, 2.218671295934095703E-30 ) ) ;
#2469=AXIS2_PLACEMENT_3D ( 'NONE', #3804, #11793, #6709 ) ;
#2477=EDGE_CURVE ( 'NONE', #4568, #6306, #10550, .T. ) ;
#2507=ORIENTED_EDGE ( 'NONE', *, *, #2018, .T. ) ;
#2510=TOROIDAL_SURFACE ( 'NONE', #12586, 2.200000000000001066, 0.2000000000000000111 ) ;
#2526=( NAMED_UNIT ( * ) PLANE_ANGLE_UNIT ( ) SI_UNIT ( $, .RADIAN. ) );
#2598=ADVANCED_FACE ( 'NONE', ( #7903 ), #5016, .F. ) ;
#2606=DIRECTION ( 'NONE',  ( -1.000000000000000000, -1.031065855027150586E-29, 2.218671295934095703E-30 ) ) ;
#2615=ORIENTED_EDGE ( 'NONE', *, *, #4106, .T. ) ;
#2621=LINE ( 'NONE', #8341, #3639 ) ;
#2623=AXIS2_PLACEMENT_3D ( 'NONE', #10831, #7817, #5882 ) ;
#2643=AXIS2_PLACEMENT_3D ( 'NONE', #9686, #4880, #11777 ) ;
#2698=DIRECTION ( 'NONE',  ( 0.000000000000000000, 5.551115123125776539E-17, 1.000000000000000000 ) ) ;
#2731=DIRECTION ( 'NONE',  ( -1.000000000000000000, -1.031065855027150586E-29, 2.218671295934095703E-30 ) ) ;
#2743=LINE ( 'NONE', #3571, #5501 ) ;
#2755=AXIS2_PLACEMENT_3D ( 'NONE', #8319, #3446, #4904 ) ;
#2759=CARTESIAN_POINT ( 'NONE',  ( 4.200000000000001954, 3.915468285211854230E-16, 2.200000000000003730 ) ) ;
#2774=EDGE_LOOP ( 'NONE', ( #6228, #9428, #5085 ) ) ;
#2808=CARTESIAN_POINT ( 'NONE',  ( 4.200000000000001954, 1.110223024630118969E-16, 2.000000000000000888 ) ) ;
#2815=DIRECTION ( 'NONE',  ( -1.000000000000000000, -1.031065855027150586E-29, 2.218671295934095703E-30 ) ) ;
#2847=ADVANCED_FACE ( 'NONE', ( #5394 ), #6357, .T. ) ;
#2889=CIRCLE ( 'NONE', #3294, 3.300000000000003375 ) ;
#2910=VECTOR ( 'NONE', #10354, 1000.000000000000114 ) ;
#2918=ORIENTED_EDGE ( 'NONE', *, *, #10760, .T. ) ;
#2920=DIRECTION ( 'NONE',  ( -7.025792437124625182E-30, -0.4999999999999992784, 0.8660254037844390407 ) ) ;
#2928=ORIENTED_EDGE ( 'NONE', *, *, #10118, .T. ) ;
#2932=CIRCLE ( 'NONE', #2307, 1.610000000000001874 ) ;
#2963=PLANE ( 'NONE',  #12215 ) ;
#2966=PLANE ( 'NONE',  #8734 ) ;
#2985=VERTEX_POINT ( 'NONE', #4688 ) ;
#2990=CARTESIAN_POINT ( 'NONE',  ( 2.000000000000001776, 1.773042676681338303, 0.000000000000000000 ) ) ;
#2993=DIRECTION ( 'NONE',  ( 0.000000000000000000, 5.551115123125776539E-17, 1.000000000000000000 ) ) ;
#2998=CARTESIAN_POINT ( 'NONE',  ( 2.000000000000001776, 0.8865213383406622683, -1.535499999999995202 ) ) ;
#3000=LINE ( 'NONE', #7928, #10723 ) ;
#3007=FACE_OUTER_BOUND ( 'NONE', #1593, .T. ) ;
#3014=ORIENTED_EDGE ( 'NONE', *, *, #4338, .F. ) ;
#3031=ORIENTED_EDGE ( 'NONE', *, *, #10270, .F. ) ;
#3048=LINE ( 'NONE', #6771, #1004 ) ;
#3066=ADVANCED_FACE ( 'NONE', ( #6819 ), #2963, .F. ) ;
#3069=DIRECTION ( 'NONE',  ( -1.000000000000000000, -1.031065855027150586E-29, 2.218671295934095703E-30 ) ) ;
#3099=EDGE_LOOP ( 'NONE', ( #7832, #5555, #8417, #6841, #4080 ) ) ;
#3128=FACE_OUTER_BOUND ( 'NONE', #11826, .T. ) ;
#3134=ORIENTED_EDGE ( 'NONE', *, *, #7001, .F. ) ;
#3135=CARTESIAN_POINT ( 'NONE',  ( 28.61000000000001009, 1.339070573674431444E-16, -2.000000000000001332 ) ) ;
#3144=ORIENTED_EDGE ( 'NONE', *, *, #838, .F. ) ;
#3158=ORIENTED_EDGE ( 'NONE', *, *, #8084, .T. ) ;
#3187=DIRECTION ( 'NONE',  ( -1.031682152609352680E-29, -1.000000000000000000, 1.498801083243958569E-15 ) ) ;
#3220=CARTESIAN_POINT ( 'NONE',  ( 0.1999999999999987899, 2.343373503925209768E-16, -3.500000000000000000 ) ) ;
#3250=DIRECTION ( 'NONE',  ( 0.000000000000000000, 5.551115123125776539E-17, 1.000000000000000000 ) ) ;
#3268=LINE ( 'NONE', #4472, #11092 ) ;
#3294=AXIS2_PLACEMENT_3D ( 'NONE', #3785, #2101, #6748 ) ;
#3307=SURFACE_SIDE_STYLE ('',( #11146 ) ) ;
#3373=CARTESIAN_POINT ( 'NONE',  ( 0.000000000000000000, 0.000000000000000000, 0.000000000000000000 ) ) ;
#3400=DIRECTION ( 'NONE',  ( -1.000000000000000000, -1.031065855027150586E-29, 2.218671295934095703E-30 ) ) ;
#3402=CARTESIAN_POINT ( 'NONE',  ( 28.99999999999999645, 3.558819905435939259E-15, 1.610000000000001874 ) ) ;
#3404=PLANE ( 'NONE',  #7342 ) ;
#3413=ORIENTED_EDGE ( 'NONE', *, *, #5811, .F. ) ;
#3421=AXIS2_PLACEMENT_3D ( 'NONE', #5133, #12748, #1974 ) ;
#3445=ORIENTED_EDGE ( 'NONE', *, *, #12352, .T. ) ;
#3446=DIRECTION ( 'NONE',  ( -1.000000000000000000, -1.031065855027150586E-29, 2.218671295934095703E-30 ) ) ;
#3460=EDGE_CURVE ( 'NONE', #10402, #10850, #922, .T. ) ;
#3479=CARTESIAN_POINT ( 'NONE',  ( 28.99999999999999645, 3.469446951953614189E-15, 0.000000000000000000 ) ) ;
#3493=CARTESIAN_POINT ( 'NONE',  ( 2.000000000000001776, -1.387778780781445676E-14, -1.535499999999974330 ) ) ;
#3506=DIRECTION ( 'NONE',  ( 2.218671295934095002E-30, 5.551115123125776539E-17, 1.000000000000000000 ) ) ;
#3558=CARTESIAN_POINT ( 'NONE',  ( 2.000000000000001776, -0.8865213383406727043, 1.535500000000009191 ) ) ;
#3571=CARTESIAN_POINT ( 'NONE',  ( 2.000000000000001776, 0.8865213383406622683, -1.535499999999995202 ) ) ;
#3576=FILL_AREA_STYLE_COLOUR ( '', #810 ) ;
#3578=FACE_BOUND ( 'NONE', #6947, .T. ) ;
#3585=FACE_OUTER_BOUND ( 'NONE', #10006, .T. ) ;
#3601=DIRECTION ( 'NONE',  ( 0.000000000000000000, -5.551115123125776539E-17, -1.000000000000000000 ) ) ;
#3610=CARTESIAN_POINT ( 'NONE',  ( 2.000000000000001776, 8.523737271559639822E-17, 1.535500000000001863 ) ) ;
#3611=ADVANCED_FACE ( 'NONE', ( #3128 ), #7077, .F. ) ;
#3622=EDGE_CURVE ( 'NONE', #11248, #10850, #2283, .T. ) ;
#3634=CARTESIAN_POINT ( 'NONE',  ( -7.321615276582515819E-30, 1.831867990631508193E-16, 3.300000000000003375 ) ) ;
#3639=VECTOR ( 'NONE', #7323, 999.9999999999998863 ) ;
#3641=DIRECTION ( 'NONE',  ( 0.000000000000000000, 5.551115123125777155E-17, 1.000000000000000000 ) ) ;
#3655=ADVANCED_FACE ( 'NONE', ( #8124 ), #9979, .F. ) ;
#3669=CARTESIAN_POINT ( 'NONE',  ( 2.000000000000001776, -1.773042676681348739, 1.387778780781445676E-14 ) ) ;
#3676=ORIENTED_EDGE ( 'NONE', *, *, #9614, .T. ) ;
#3682=AXIS2_PLACEMENT_3D ( 'NONE', #5524, #10339, #3601 ) ;
#3707=DIRECTION ( 'NONE',  ( -1.000000000000000000, -1.031065855027150586E-29, 2.218671295934095703E-30 ) ) ;
#3709=DIRECTION ( 'NONE',  ( 2.218671295934095002E-30, 5.551115123125776539E-17, 1.000000000000000000 ) ) ;
#3716=VERTEX_POINT ( 'NONE', #5296 ) ;
#3785=CARTESIAN_POINT ( 'NONE',  ( 0.000000000000000000, 0.000000000000000000, 0.000000000000000000 ) ) ;
#3804=CARTESIAN_POINT ( 'NONE',  ( 2.000000000000001776, 1.773042676681338303, 0.000000000000000000 ) ) ;
#3820=AXIS2_PLACEMENT_3D ( 'NONE', #9734, #3069, #4017 ) ;
#3825=ADVANCED_FACE ( 'NONE', ( #6395 ), #5634, .T. ) ;
#3849=LINE ( 'NONE', #5001, #7989 ) ;
#3874=DIRECTION ( 'NONE',  ( -1.000000000000000000, -1.031065855027150586E-29, 2.218671295934095703E-30 ) ) ;
#3898=CARTESIAN_POINT ( 'NONE',  ( 3.999999999999999112, -1.221245327087693494E-16, -2.200000000000003730 ) ) ;
#3907=CONICAL_SURFACE ( 'NONE', #8425, 1.535500000000001863, 1.047197551196590748 ) ;
#3914=ORIENTED_EDGE ( 'NONE', *, *, #4728, .F. ) ;
#3962=CARTESIAN_POINT ( 'NONE',  ( 3.999999999999999112, 3.915468285211833029E-16, 2.200000000000003730 ) ) ;
#3979=ORIENTED_EDGE ( 'NONE', *, *, #1551, .F. ) ;
#3981=AXIS2_PLACEMENT_3D ( 'NONE', #7110, #1174, #6198 ) ;
#4007=CARTESIAN_POINT ( 'NONE',  ( 2.000000000000001776, -0.8865213383406761460, -1.535499999999995202 ) ) ;
#4013=CARTESIAN_POINT ( 'NONE',  ( 28.99999999999999645, 1.610000000000000320, 2.775557561562891351E-14 ) ) ;
#4016=ORIENTED_EDGE ( 'NONE', *, *, #5344, .F. ) ;
#4017=DIRECTION ( 'NONE',  ( 0.000000000000000000, 5.551115123125776539E-17, 1.000000000000000000 ) ) ;
#4070=FACE_BOUND ( 'NONE', #9389, .T. ) ;
#4071=CARTESIAN_POINT ( 'NONE',  ( 4.200000000000001954, 0.000000000000000000, 0.000000000000000000 ) ) ;
#4076=FACE_OUTER_BOUND ( 'NONE', #8667, .T. ) ;
#4080=ORIENTED_EDGE ( 'NONE', *, *, #2301, .T. ) ;
#4084=ORIENTED_EDGE ( 'NONE', *, *, #2477, .T. ) ;
#4093=LINE ( 'NONE', #9574, #9236 ) ;
#4106=EDGE_CURVE ( 'NONE', #6292, #1618, #4404, .T. ) ;
#4186=AXIS2_PLACEMENT_3D ( 'NONE', #4071, #7992, #10047 ) ;
#4187=VERTEX_POINT ( 'NONE', #7460 ) ;
#4197=CARTESIAN_POINT ( 'NONE',  ( -31.74999999999995026, 1.339070573669553325E-16, -1.999999999999996225 ) ) ;
#4210=DIRECTION ( 'NONE',  ( 1.031065855027150586E-29, -1.000000000000000000, 5.551115123125776539E-17 ) ) ;
#4215=ORIENTED_EDGE ( 'NONE', *, *, #5869, .F. ) ;
#4225=CARTESIAN_POINT ( 'NONE',  ( 4.200000000000001954, 1.339070573674521670E-16, -2.000000000000000888 ) ) ;
#4238=AXIS2_PLACEMENT_3D ( 'NONE', #1416, #10035, #8114 ) ;
#4247=TOROIDAL_SURFACE ( 'NONE', #6726, 3.299999999999999822, 0.2000000000000000111 ) ;
#4260=DIRECTION ( 'NONE',  ( -1.000000000000000000, -1.031065855027150586E-29, 2.218671295934095703E-30 ) ) ;
#4286=ADVANCED_FACE ( 'NONE', ( #8741 ), #5095, .T. ) ;
#4307=DIRECTION ( 'NONE',  ( 0.000000000000000000, 5.551115123125776539E-17, 1.000000000000000000 ) ) ;
#4338=EDGE_CURVE ( 'NONE', #1582, #6684, #1972, .T. ) ;
#4354=DIRECTION ( 'NONE',  ( -1.031065855027150586E-29, 1.000000000000000000, 6.695352868347756765E-17 ) ) ;
#4371=CLOSED_SHELL ( 'NONE', ( #9615, #5836, #3611, #2847, #7179, #7071, #56, #966, #11280, #2403, #4286, #6045, #11328, #3825, #10066, #9186, #6828, #4630, #6036, #3066, #10927, #9412, #2598, #12044, #4874, #3655, #5412 ) ) ;
#4376=PRODUCT_DEFINITION ( 'UNKNOWN', '', #1585, #1990 ) ;
#4404=CIRCLE ( 'NONE', #9325, 3.500000000000003997 ) ;
#4421=AXIS2_PLACEMENT_3D ( 'NONE', #5787, #11726, #9700 ) ;
#4435=EDGE_CURVE ( 'NONE', #1618, #9867, #7839, .T. ) ;
#4436=SHAPE_REPRESENTATION ( 'socket head cap screw_iso_ISO 4762 M4 x 25 - 25N', ( #12422 ), #7637 ) ;
#4472=CARTESIAN_POINT ( 'NONE',  ( 2.000000000000001776, -1.773042676681348739, 1.387778780781445676E-14 ) ) ;
#4475=ORIENTED_EDGE ( 'NONE', *, *, #3460, .F. ) ;
#4509=DIRECTION ( 'NONE',  ( 0.000000000000000000, 5.551115123125776539E-17, 1.000000000000000000 ) ) ;
#4550=CARTESIAN_POINT ( 'NONE',  ( 2.000000000000001776, -1.773042676681348739, 1.387778780781445676E-14 ) ) ;
#4558=DIRECTION ( 'NONE',  ( 1.000000000000000000, 1.031065855027150586E-29, 2.218671295934092550E-30 ) ) ;
#4568=VERTEX_POINT ( 'NONE', #5379 ) ;
#4571=LINE ( 'NONE', #3669, #8333 ) ;
#4585=DIRECTION ( 'NONE',  ( 0.000000000000000000, 5.551115123125776539E-17, 1.000000000000000000 ) ) ;
#4586=EDGE_LOOP ( 'NONE', ( #6506, #2383, #10324 ) ) ;
#4596=DIRECTION ( 'NONE',  ( -1.031065855027149465E-29, -1.000000000000000000, 7.771561172376086908E-16 ) ) ;
#4598=EDGE_CURVE ( 'NONE', #271, #10402, #2621, .T. ) ;
#4630=ADVANCED_FACE ( 'NONE', ( #8464 ), #3404, .T. ) ;
#4650=ORIENTED_EDGE ( 'NONE', *, *, #9514, .F. ) ;
#4682=EDGE_CURVE ( 'NONE', #11248, #7729, #5445, .T. ) ;
#4688=CARTESIAN_POINT ( 'NONE',  ( 2.000000000000001776, -0.8865213383406761460, -1.535499999999995202 ) ) ;
#4728=EDGE_CURVE ( 'NONE', #9867, #1053, #8968, .T. ) ;
#4766=EDGE_LOOP ( 'NONE', ( #2177, #3979, #10529 ) ) ;
#4810=EDGE_LOOP ( 'NONE', ( #791, #5026, #1647, #3134 ) ) ;
#4825=CARTESIAN_POINT ( 'NONE',  ( 2.000000000000001776, 1.773042676681338303, 0.000000000000000000 ) ) ;
#4839=LINE ( 'NONE', #1933, #9649 ) ;
#4855=LINE ( 'NONE', #9729, #2204 ) ;
#4874=ADVANCED_FACE ( 'NONE', ( #10706 ), #10768, .F. ) ;
#4880=DIRECTION ( 'NONE',  ( -1.000000000000000000, -1.031065855027150586E-29, 2.218671295934095703E-30 ) ) ;
#4884=CONICAL_SURFACE ( 'NONE', #7150, 1.535500000000001863, 1.047197551196590748 ) ;
#4904=DIRECTION ( 'NONE',  ( 0.000000000000000000, 5.551115123125776539E-17, 1.000000000000000000 ) ) ;
#4907=CARTESIAN_POINT ( 'NONE',  ( 0.000000000000000000, 0.8865213383406657099, 1.535500000000022958 ) ) ;
#4918=CARTESIAN_POINT ( 'NONE',  ( 2.000000000000001776, 0.8865213383406622683, -1.535499999999995202 ) ) ;
#4926=DIRECTION ( 'NONE',  ( 1.000000000000000000, 1.031065855027150586E-29, -2.218671295934095703E-30 ) ) ;
#4990=DIRECTION ( 'NONE',  ( 7.038118388768704892E-30, 0.4999999999999992784, -0.8660254037844390407 ) ) ;
#5001=CARTESIAN_POINT ( 'NONE',  ( 2.000000000000001776, -0.8865213383406727043, 1.535500000000009191 ) ) ;
#5016=PLANE ( 'NONE',  #5327 ) ;
#5026=ORIENTED_EDGE ( 'NONE', *, *, #11372, .T. ) ;
#5034=EDGE_CURVE ( 'NONE', #5244, #11248, #7305, .T. ) ;
#5036=DIRECTION ( 'NONE',  ( -1.000000000000000000, -1.031065855027150586E-29, 2.218671295934095703E-30 ) ) ;
#5046=VECTOR ( 'NONE', #10072, 1000.000000000000114 ) ;
#5057=VERTEX_POINT ( 'NONE', #3634 ) ;
#5058=CIRCLE ( 'NONE', #6078, 0.2000000000000000944 ) ;
#5063=PRODUCT_CONTEXT ( 'NONE', #6331, 'mechanical' ) ;
#5079=VERTEX_POINT ( 'NONE', #7489 ) ;
#5085=ORIENTED_EDGE ( 'NONE', *, *, #2334, .F. ) ;
#5095=CONICAL_SURFACE ( 'NONE', #2643, 1.610000000000001874, 0.7853981633974658205 ) ;
#5099=FACE_OUTER_BOUND ( 'NONE', #1343, .T. ) ;
#5131=DIRECTION ( 'NONE',  ( -1.000000000000000000, -1.031065855027150586E-29, 2.218671295934095703E-30 ) ) ;
#5133=CARTESIAN_POINT ( 'NONE',  ( 2.000000000000001776, 0.000000000000000000, 0.000000000000000000 ) ) ;
#5162=CARTESIAN_POINT ( 'NONE',  ( -31.74999999999995026, 0.000000000000000000, 6.938893903907228378E-15 ) ) ;
#5220=( NAMED_UNIT ( * ) SI_UNIT ( $, .STERADIAN. ) SOLID_ANGLE_UNIT ( ) );
#5244=VERTEX_POINT ( 'NONE', #910 ) ;
#5296=CARTESIAN_POINT ( 'NONE',  ( -7.321615276582520023E-30, 2.276419975238227341E-16, -3.299999999999999822 ) ) ;
#5327=AXIS2_PLACEMENT_3D ( 'NONE', #4825, #10670, #5722 ) ;
#5337=( GEOMETRIC_REPRESENTATION_CONTEXT ( 3 ) GLOBAL_UNCERTAINTY_ASSIGNED_CONTEXT ( ( #9534 ) ) GLOBAL_UNIT_ASSIGNED_CONTEXT ( ( #1882, #6665, #10572 ) ) REPRESENTATION_CONTEXT ( 'NONE', 'WORKASPACE' ) );
#5344=EDGE_CURVE ( 'NONE', #1618, #6292, #1587, .T. ) ;
#5379=CARTESIAN_POINT ( 'NONE',  ( 0.000000000000000000, -1.773042676681359175, 1.387778780781445676E-14 ) ) ;
#5381=CARTESIAN_POINT ( 'NONE',  ( 0.1999999999999987899, 2.209466446554762247E-16, -3.300000000000003375 ) ) ;
#5383=CARTESIAN_POINT ( 'NONE',  ( 0.1999999999999987899, 1.942890293094023946E-16, 3.500000000000003997 ) ) ;
#5394=FACE_OUTER_BOUND ( 'NONE', #8377, .T. ) ;
#5412=ADVANCED_FACE ( 'NONE', ( #5099 ), #4884, .F. ) ;
#5430=DIRECTION ( 'NONE',  ( -1.031065855027149465E-29, -1.000000000000000000, 7.771561172376086908E-16 ) ) ;
#5445=LINE ( 'NONE', #9354, #10814 ) ;
#5501=VECTOR ( 'NONE', #4596, 1000.000000000000000 ) ;
#5513=CARTESIAN_POINT ( 'NONE',  ( -31.74999999999995026, 0.000000000000000000, 6.938893903907228378E-15 ) ) ;
#5524=CARTESIAN_POINT ( 'NONE',  ( 4.200000000000001954, 0.000000000000000000, 0.000000000000000000 ) ) ;
#5555=ORIENTED_EDGE ( 'NONE', *, *, #5034, .F. ) ;
#5557=CARTESIAN_POINT ( 'NONE',  ( 0.1999999999999987899, 0.000000000000000000, 0.000000000000000000 ) ) ;
#5565=FILL_AREA_STYLE ('',( #3576 ) ) ;
#5586=ORIENTED_EDGE ( 'NONE', *, *, #8399, .T. ) ;
#5634=TOROIDAL_SURFACE ( 'NONE', #281, 3.299999999999999822, 0.2000000000000000111 ) ;
#5641=VECTOR ( 'NONE', #5430, 1000.000000000000000 ) ;
#5647=DIRECTION ( 'NONE',  ( 3.260214209858708648E-30, 0.5000000000000012212, 0.8660254037844379305 ) ) ;
#5665=CARTESIAN_POINT ( 'NONE',  ( 2.000000000000001776, 0.000000000000000000, 0.000000000000000000 ) ) ;
#5681=DIRECTION ( 'NONE',  ( 0.000000000000000000, 5.551115123125776539E-17, 1.000000000000000000 ) ) ;
#5696=CARTESIAN_POINT ( 'NONE',  ( 2.000000000000001776, 1.773042676681338303, 0.000000000000000000 ) ) ;
#5707=CARTESIAN_POINT ( 'NONE',  ( 0.000000000000000000, 0.000000000000000000, 0.000000000000000000 ) ) ;
#5715=DIRECTION ( 'NONE',  ( 1.031682152609352680E-29, 1.000000000000000000, -1.498801083243958569E-15 ) ) ;
#5722=DIRECTION ( 'NONE',  ( 2.218671295934093250E-30, -5.551115123125776539E-17, -1.000000000000000000 ) ) ;
#5734=ORIENTED_EDGE ( 'NONE', *, *, #6884, .F. ) ;
#5746=CARTESIAN_POINT ( 'NONE',  ( 2.000000000000001776, 0.000000000000000000, 0.000000000000000000 ) ) ;
#5787=CARTESIAN_POINT ( 'NONE',  ( 3.999999999999996447, 0.000000000000000000, 0.000000000000000000 ) ) ;
#5811=EDGE_CURVE ( 'NONE', #93, #1090, #12220, .T. ) ;
#5826=ORIENTED_EDGE ( 'NONE', *, *, #3622, .F. ) ;
#5836=ADVANCED_FACE ( 'NONE', ( #3585 ), #4247, .T. ) ;
#5869=EDGE_CURVE ( 'NONE', #7720, #11206, #10418, .T. ) ;
#5882=DIRECTION ( 'NONE',  ( 1.031065855027149465E-29, 1.000000000000000000, -7.771561172376086908E-16 ) ) ;
#5892=CARTESIAN_POINT ( 'NONE',  ( 2.000000000000001776, -1.329782007511014275, 0.7677500000000114788 ) ) ;
#5906=AXIS2_PLACEMENT_3D ( 'NONE', #10884, #5036, #2993 ) ;
#5911=ORIENTED_EDGE ( 'NONE', *, *, #2301, .F. ) ;
#5968=DIRECTION ( 'NONE',  ( -1.000000000000000000, -1.031065855027150586E-29, 2.218671295934095703E-30 ) ) ;
#6009=AXIS2_PLACEMENT_3D ( 'NONE', #7028, #8820, #6842 ) ;
#6011=EDGE_CURVE ( 'NONE', #5079, #7729, #4855, .T. ) ;
#6013=CARTESIAN_POINT ( 'NONE',  ( 2.000000000000001776, 1.773042676681338303, 0.000000000000000000 ) ) ;
#6025=DIRECTION ( 'NONE',  ( -1.000000000000000000, -1.031065855027150586E-29, 2.218671295934095703E-30 ) ) ;
#6036=ADVANCED_FACE ( 'NONE', ( #7874 ), #12724, .F. ) ;
#6045=ADVANCED_FACE ( 'NONE', ( #3007 ), #1042, .T. ) ;
#6078=AXIS2_PLACEMENT_3D ( 'NONE', #7246, #4210, #341 ) ;
#6111=VECTOR ( 'NONE', #2606, 1000.000000000000000 ) ;
#6185=CYLINDRICAL_SURFACE ( 'NONE', #11938, 2.000000000000003109 ) ;
#6198=DIRECTION ( 'NONE',  ( 2.218671295934093250E-30, -5.551115123125776539E-17, -1.000000000000000000 ) ) ;
#6199=DIRECTION ( 'NONE',  ( 2.218671295934093250E-30, -5.551115123125776539E-17, -1.000000000000000000 ) ) ;
#6217=CYLINDRICAL_SURFACE ( 'NONE', #6373, 3.500000000000003997 ) ;
#6228=ORIENTED_EDGE ( 'NONE', *, *, #4598, .T. ) ;
#6236=DIRECTION ( 'NONE',  ( 0.000000000000000000, 5.551115123125776539E-17, 1.000000000000000000 ) ) ;
#6267=EDGE_CURVE ( 'NONE', #10402, #7997, #2743, .T. ) ;
#6276=AXIS2_PLACEMENT_3D ( 'NONE', #5381, #4354, #12289 ) ;
#6292=VERTEX_POINT ( 'NONE', #10631 ) ;
#6306=VERTEX_POINT ( 'NONE', #11865 ) ;
#6330=CARTESIAN_POINT ( 'NONE',  ( 0.000000000000000000, -0.8865213383406727043, 1.535500000000009191 ) ) ;
#6331=APPLICATION_CONTEXT ( 'automotive_design' ) ;
#6357=CONICAL_SURFACE ( 'NONE', #2256, 1.610000000000001874, 0.7853981633974658205 ) ;
#6369=EDGE_CURVE ( 'NONE', #1582, #10108, #9655, .T. ) ;
#6372=ORIENTED_EDGE ( 'NONE', *, *, #6369, .F. ) ;
#6373=AXIS2_PLACEMENT_3D ( 'NONE', #2304, #5131, #7322 ) ;
#6395=FACE_OUTER_BOUND ( 'NONE', #96, .T. ) ;
#6428=DIRECTION ( 'NONE',  ( 1.000000000000000000, 0.000000000000000000, 0.000000000000000000 ) ) ;
#6438=AXIS2_PLACEMENT_3D ( 'NONE', #7043, #9916, #336 ) ;
#6506=ORIENTED_EDGE ( 'NONE', *, *, #7176, .F. ) ;
#6539=CARTESIAN_POINT ( 'NONE',  ( 4.200000000000001954, 0.000000000000000000, 0.000000000000000000 ) ) ;
#6541=ORIENTED_EDGE ( 'NONE', *, *, #5344, .T. ) ;
#6545=DIRECTION ( 'NONE',  ( 0.000000000000000000, 1.779758311459930245E-16, 1.000000000000000000 ) ) ;
#6588=AXIS2_PLACEMENT_3D ( 'NONE', #5665, #12509, #4585 ) ;
#6655=EDGE_CURVE ( 'NONE', #9867, #5057, #11622, .T. ) ;
#6665=( NAMED_UNIT ( * ) PLANE_ANGLE_UNIT ( ) SI_UNIT ( $, .RADIAN. ) );
#6684=VERTEX_POINT ( 'NONE', #7717 ) ;
#6686=AXIS2_PLACEMENT_3D ( 'NONE', #2017, #4926, #6866 ) ;
#6697=CIRCLE ( 'NONE', #4421, 2.200000000000003730 ) ;
#6703=ORIENTED_EDGE ( 'NONE', *, *, #382, .F. ) ;
#6709=DIRECTION ( 'NONE',  ( 2.218671295934093250E-30, -5.551115123125776539E-17, -1.000000000000000000 ) ) ;
#6726=AXIS2_PLACEMENT_3D ( 'NONE', #12534, #7563, #3709 ) ;
#6748=DIRECTION ( 'NONE',  ( -2.218671295934093601E-30, 5.551115123125776539E-17, 1.000000000000000000 ) ) ;
#6771=CARTESIAN_POINT ( 'NONE',  ( 28.99999999999999645, 3.577242133134013559E-15, -1.610000000000001874 ) ) ;
#6819=FACE_OUTER_BOUND ( 'NONE', #12166, .T. ) ;
#6828=ADVANCED_FACE ( 'NONE', ( #7840 ), #2966, .T. ) ;
#6841=ORIENTED_EDGE ( 'NONE', *, *, #838, .T. ) ;
#6842=DIRECTION ( 'NONE',  ( 2.218671295934093250E-30, -5.551115123125776539E-17, -1.000000000000000000 ) ) ;
#6866=DIRECTION ( 'NONE',  ( 0.000000000000000000, 5.551115123125776539E-17, 1.000000000000000000 ) ) ;
#6884=EDGE_CURVE ( 'NONE', #10108, #6684, #8945, .T. ) ;
#6944=CARTESIAN_POINT ( 'NONE',  ( 2.000000000000001776, -0.8865213383406727043, 1.535500000000009191 ) ) ;
#6947=EDGE_LOOP ( 'NONE', ( #9302, #3158 ) ) ;
#6966=EDGE_CURVE ( 'NONE', #7469, #7997, #11250, .T. ) ;
#6990=ORIENTED_EDGE ( 'NONE', *, *, #9338, .T. ) ;
#7001=EDGE_CURVE ( 'NONE', #7272, #1090, #1541, .T. ) ;
#7003=EDGE_CURVE ( 'NONE', #1053, #3716, #11003, .T. ) ;
#7028=CARTESIAN_POINT ( 'NONE',  ( 2.000000000000001776, 1.773042676681338303, 0.000000000000000000 ) ) ;
#7043=CARTESIAN_POINT ( 'NONE',  ( 0.000000000000000000, 0.000000000000000000, 0.000000000000000000 ) ) ;
#7071=ADVANCED_FACE ( 'NONE', ( #10647 ), #1645, .T. ) ;
#7077=TOROIDAL_SURFACE ( 'NONE', #4186, 2.200000000000001066, 0.2000000000000000111 ) ;
#7096=DIRECTION ( 'NONE',  ( -1.000000000000000000, -1.031065855027150586E-29, 2.218671295934095703E-30 ) ) ;
#7104=DIRECTION ( 'NONE',  ( -1.000000000000000000, -1.031065855027150586E-29, 2.218671295934095703E-30 ) ) ;
#7110=CARTESIAN_POINT ( 'NONE',  ( 2.000000000000001776, 1.773042676681338303, 0.000000000000000000 ) ) ;
#7116=PLANE ( 'NONE',  #8001 ) ;
#7150=AXIS2_PLACEMENT_3D ( 'NONE', #200, #1033, #3250 ) ;
#7159=VECTOR ( 'NONE', #5968, 1000.000000000000000 ) ;
#7176=EDGE_CURVE ( 'NONE', #5244, #4187, #928, .T. ) ;
#7179=ADVANCED_FACE ( 'NONE', ( #4076 ), #1894, .T. ) ;
#7222=PLANE ( 'NONE',  #387 ) ;
#7226=SURFACE_STYLE_USAGE ( .BOTH. , #3307 ) ;
#7246=CARTESIAN_POINT ( 'NONE',  ( 4.200000000000001954, -1.221245327087672786E-16, -2.200000000000003730 ) ) ;
#7251=CARTESIAN_POINT ( 'NONE',  ( 0.000000000000000000, 1.773042676681338303, 0.000000000000000000 ) ) ;
#7272=VERTEX_POINT ( 'NONE', #3135 ) ;
#7285=FILL_AREA_STYLE_COLOUR ( '', #2079 ) ;
#7305=LINE ( 'NONE', #11290, #6111 ) ;
#7321=DIRECTION ( 'NONE',  ( -0.7071067811865348052, 3.925231146708775397E-17, 0.7071067811865602293 ) ) ;
#7322=DIRECTION ( 'NONE',  ( 0.000000000000000000, 5.551115123125776539E-17, 1.000000000000000000 ) ) ;
#7323=DIRECTION ( 'NONE',  ( -3.260214209858708648E-30, -0.5000000000000012212, -0.8660254037844380415 ) ) ;
#7342=AXIS2_PLACEMENT_3D ( 'NONE', #4550, #10256, #11247 ) ;
#7362=EDGE_CURVE ( 'NONE', #1057, #8600, #5058, .T. ) ;
#7375=ORIENTED_EDGE ( 'NONE', *, *, #6267, .F. ) ;
#7384=CARTESIAN_POINT ( 'NONE',  ( 2.000000000000001776, 1.028071432934799421E-16, -1.535500000000001863 ) ) ;
#7389=ORIENTED_EDGE ( 'NONE', *, *, #10112, .F. ) ;
#7392=DIRECTION ( 'NONE',  ( 0.000000000000000000, 0.000000000000000000, 1.000000000000000000 ) ) ;
#7410=( LENGTH_UNIT ( ) NAMED_UNIT ( * ) SI_UNIT ( .MILLI., .METRE. ) );
#7436=ORIENTED_EDGE ( 'NONE', *, *, #4435, .F. ) ;
#7460=CARTESIAN_POINT ( 'NONE',  ( 2.000000000000001776, 1.329782007511000286, 0.7677500000000045954 ) ) ;
#7469=VERTEX_POINT ( 'NONE', #8581 ) ;
#7475=DIRECTION ( 'NONE',  ( -2.218671295934093601E-30, 5.551115123125776539E-17, 1.000000000000000000 ) ) ;
#7485=APPLICATION_CONTEXT ( 'automotive_design' ) ;
#7489=CARTESIAN_POINT ( 'NONE',  ( 0.000000000000000000, -0.8865213383406727043, 1.535500000000009191 ) ) ;
#7504=DIRECTION ( 'NONE',  ( -7.025792437124625182E-30, -0.4999999999999992784, 0.8660254037844390407 ) ) ;
#7524=DIRECTION ( 'NONE',  ( 0.000000000000000000, -5.551115123125770376E-17, -1.000000000000000000 ) ) ;
#7526=DIRECTION ( 'NONE',  ( -0.5000000000000056621, 4.807406715958370281E-17, 0.8660254037844352659 ) ) ;
#7535=AXIS2_PLACEMENT_3D ( 'NONE', #1704, #9543, #12222 ) ;
#7563=DIRECTION ( 'NONE',  ( -1.000000000000000000, -1.031065855027150586E-29, 2.218671295934095703E-30 ) ) ;
#7591=DIRECTION ( 'NONE',  ( -1.000000000000000000, -1.031065855027150586E-29, 2.218671295934095703E-30 ) ) ;
#7618=VECTOR ( 'NONE', #7526, 1000.000000000000114 ) ;
#7637=( GEOMETRIC_REPRESENTATION_CONTEXT ( 3 ) GLOBAL_UNCERTAINTY_ASSIGNED_CONTEXT ( ( #8550 ) ) GLOBAL_UNIT_ASSIGNED_CONTEXT ( ( #9200, #1476, #5220 ) ) REPRESENTATION_CONTEXT ( 'NONE', 'WORKASPACE' ) );
#7674=AXIS2_PLACEMENT_3D ( 'NONE', #10610, #7591, #4509 ) ;
#7702=ORIENTED_EDGE ( 'NONE', *, *, #1676, .F. ) ;
#7717=CARTESIAN_POINT ( 'NONE',  ( 2.000000000000001776, 0.000000000000000000, 1.535500000000002085 ) ) ;
#7720=VERTEX_POINT ( 'NONE', #2808 ) ;
#7727=VECTOR ( 'NONE', #1829, 1000.000000000000114 ) ;
#7729=VERTEX_POINT ( 'NONE', #4907 ) ;
#7754=EDGE_LOOP ( 'NONE', ( #2195, #9692, #9931, #1764 ) ) ;
#7759=DIRECTION ( 'NONE',  ( 1.000000000000000000, 1.031065855027150586E-29, 2.218671295934092550E-30 ) ) ;
#7782=EDGE_CURVE ( 'NONE', #8600, #11206, #9743, .T. ) ;
#7792=VECTOR ( 'NONE', #3400, 1000.000000000000000 ) ;
#7817=DIRECTION ( 'NONE',  ( 2.206345344290014591E-30, -7.771561172376086908E-16, -1.000000000000000000 ) ) ;
#7832=ORIENTED_EDGE ( 'NONE', *, *, #4682, .F. ) ;
#7839=LINE ( 'NONE', #7892, #7159 ) ;
#7840=FACE_OUTER_BOUND ( 'NONE', #380, .T. ) ;
#7874=FACE_OUTER_BOUND ( 'NONE', #935, .T. ) ;
#7887=DIRECTION ( 'NONE',  ( -1.000000000000000000, -1.031065855027150586E-29, 2.218671295934095703E-30 ) ) ;
#7892=CARTESIAN_POINT ( 'NONE',  ( -31.74999999999995026, 1.942890293094023946E-16, 3.500000000000011102 ) ) ;
#7903=FACE_OUTER_BOUND ( 'NONE', #12102, .T. ) ;
#7910=ORIENTED_EDGE ( 'NONE', *, *, #6884, .T. ) ;
#7919=DIRECTION ( 'NONE',  ( -3.260214209858708648E-30, -0.5000000000000012212, -0.8660254037844380415 ) ) ;
#7928=CARTESIAN_POINT ( 'NONE',  ( -31.74999999999995026, 2.343373503921717580E-16, -3.499999999999996891 ) ) ;
#7933=DIRECTION ( 'NONE',  ( 1.000000000000000000, 1.031065855027150586E-29, 2.218671295934092550E-30 ) ) ;
#7952=DIRECTION ( 'NONE',  ( 0.000000000000000000, 5.551115123125777772E-17, 1.000000000000000000 ) ) ;
#7973=DIRECTION ( 'NONE',  ( 0.000000000000000000, -5.551115123125776539E-17, -1.000000000000000000 ) ) ;
#7989=VECTOR ( 'NONE', #10721, 999.9999999999998863 ) ;
#7992=DIRECTION ( 'NONE',  ( 1.000000000000000000, 1.031065855027150586E-29, -2.218671295934095703E-30 ) ) ;
#7997=VERTEX_POINT ( 'NONE', #3493 ) ;
#7998=CARTESIAN_POINT ( 'NONE',  ( 2.000000000000001776, 1.773042676681338303, 0.000000000000000000 ) ) ;
#8001=AXIS2_PLACEMENT_3D ( 'NONE', #6013, #1052, #4990 ) ;
#8044=DIRECTION ( 'NONE',  ( 0.000000000000000000, 5.551115123125776539E-17, 1.000000000000000000 ) ) ;
#8049=DIRECTION ( 'NONE',  ( -2.243323199222248468E-30, 1.498801083243958569E-15, 1.000000000000000000 ) ) ;
#8084=EDGE_CURVE ( 'NONE', #11206, #8600, #6697, .T. ) ;
#8087=ORIENTED_EDGE ( 'NONE', *, *, #3622, .T. ) ;
#8114=DIRECTION ( 'NONE',  ( 0.000000000000000000, -5.551115123125775923E-17, -1.000000000000000000 ) ) ;
#8124=FACE_OUTER_BOUND ( 'NONE', #2774, .T. ) ;
#8221=ORIENTED_EDGE ( 'NONE', *, *, #342, .T. ) ;
#8233=EDGE_LOOP ( 'NONE', ( #4215, #960, #2358, #10780 ) ) ;
#8283=ORIENTED_EDGE ( 'NONE', *, *, #10112, .T. ) ;
#8287=ORIENTED_EDGE ( 'NONE', *, *, #9614, .F. ) ;
#8290=ORIENTED_EDGE ( 'NONE', *, *, #1500, .T. ) ;
#8319=CARTESIAN_POINT ( 'NONE',  ( 2.000000000000001776, 0.000000000000000000, 0.000000000000000000 ) ) ;
#8328=PRODUCT ( 'socket head cap screw_iso_ISO 4762 M4 x 25 - 25N', 'socket head cap screw_iso_ISO 4762 M4 x 25 - 25N', '', ( #5063 ) ) ;
#8333=VECTOR ( 'NONE', #9374, 1000.000000000000114 ) ;
#8336=ORIENTED_EDGE ( 'NONE', *, *, #4106, .F. ) ;
#8341=CARTESIAN_POINT ( 'NONE',  ( 2.000000000000001776, 1.773042676681338303, 0.000000000000000000 ) ) ;
#8343=DIRECTION ( 'NONE',  ( 0.000000000000000000, 5.551115123125777772E-17, 1.000000000000000000 ) ) ;
#8376=LINE ( 'NONE', #3558, #9425 ) ;
#8377=EDGE_LOOP ( 'NONE', ( #2507, #2918, #9239, #3413 ) ) ;
#8399=EDGE_CURVE ( 'NONE', #10778, #10168, #4571, .T. ) ;
#8404=DIRECTION ( 'NONE',  ( -1.000000000000000000, -1.031065855027150586E-29, 2.218671295934095703E-30 ) ) ;
#8417=ORIENTED_EDGE ( 'NONE', *, *, #7176, .T. ) ;
#8425=AXIS2_PLACEMENT_3D ( 'NONE', #12051, #378, #4307 ) ;
#8430=ORIENTED_EDGE ( 'NONE', *, *, #11372, .F. ) ;
#8456=CARTESIAN_POINT ( 'NONE',  ( 28.99999999999999645, 3.469446951953614189E-15, 0.000000000000000000 ) ) ;
#8464=FACE_OUTER_BOUND ( 'NONE', #9633, .T. ) ;
#8470=DIRECTION ( 'NONE',  ( 2.218671295934093250E-30, -5.551115123125776539E-17, -1.000000000000000000 ) ) ;
#8481=CARTESIAN_POINT ( 'NONE',  ( 0.1999999999999987899, 1.831867990631508193E-16, 3.300000000000003375 ) ) ;
#8524=EDGE_CURVE ( 'NONE', #7997, #2985, #11527, .T. ) ;
#8550=UNCERTAINTY_MEASURE_WITH_UNIT (LENGTH_MEASURE( 1.000000000000000082E-05 ), #9200, 'distance_accuracy_value', 'NONE');
#8561=EDGE_CURVE ( 'NONE', #1053, #9867, #494, .T. ) ;
#8581=CARTESIAN_POINT ( 'NONE',  ( 2.886521338340684917, 0.000000000000000000, 0.000000000000000000 ) ) ;
#8597=ORIENTED_EDGE ( 'NONE', *, *, #8614, .T. ) ;
#8600=VERTEX_POINT ( 'NONE', #3898 ) ;
#8614=EDGE_CURVE ( 'NONE', #10850, #6306, #1115, .T. ) ;
#8626=AXIS2_PLACEMENT_3D ( 'NONE', #5746, #1759, #5681 ) ;
#8652=SURFACE_SIDE_STYLE ('',( #9533 ) ) ;
#8656=ORIENTED_EDGE ( 'NONE', *, *, #9775, .T. ) ;
#8667=EDGE_LOOP ( 'NONE', ( #1731, #980, #2058, #1837 ) ) ;
#8719=ORIENTED_EDGE ( 'NONE', *, *, #8561, .T. ) ;
#8734=AXIS2_PLACEMENT_3D ( 'NONE', #11704, #11839, #1911 ) ;
#8741=FACE_OUTER_BOUND ( 'NONE', #4810, .T. ) ;
#8772=DIRECTION ( 'NONE',  ( -1.000000000000000000, -1.031065855027150586E-29, 2.218671295934095703E-30 ) ) ;
#8775=CARTESIAN_POINT ( 'NONE',  ( -31.74999999999995026, 1.110223024625157033E-16, 2.000000000000010214 ) ) ;
#8795=VECTOR ( 'NONE', #5715, 1000.000000000000000 ) ;
#8820=DIRECTION ( 'NONE',  ( 1.000000000000000000, 1.031065855027150586E-29, 2.218671295934092550E-30 ) ) ;
#8833=AXIS2_PLACEMENT_3D ( 'NONE', #2231, #7887, #10063 ) ;
#8860=ORIENTED_EDGE ( 'NONE', *, *, #6011, .F. ) ;
#8878=PLANE ( 'NONE',  #2469 ) ;
#8885=LINE ( 'NONE', #2990, #11148 ) ;
#8934=ORIENTED_EDGE ( 'NONE', *, *, #8561, .F. ) ;
#8945=CIRCLE ( 'NONE', #3421, 1.535500000000001863 ) ;
#8968=CIRCLE ( 'NONE', #7535, 3.500000000000003997 ) ;
#8969=CARTESIAN_POINT ( 'NONE',  ( 0.000000000000000000, 0.8865213383406622683, -1.535499999999995202 ) ) ;
#8972=ORIENTED_EDGE ( 'NONE', *, *, #2477, .F. ) ;
#8999=CARTESIAN_POINT ( 'NONE',  ( 4.000000000000003553, 0.000000000000000000, 0.000000000000000000 ) ) ;
#9051=CARTESIAN_POINT ( 'NONE',  ( 28.61000000000001009, 3.469446951953614189E-15, 0.000000000000000000 ) ) ;
#9068=ORIENTED_EDGE ( 'NONE', *, *, #2334, .T. ) ;
#9089=PLANE ( 'NONE',  #6438 ) ;
#9131=CARTESIAN_POINT ( 'NONE',  ( 2.000000000000001776, -0.8865213383406727043, 1.535500000000009191 ) ) ;
#9152=CARTESIAN_POINT ( 'NONE',  ( 28.99999999999999645, 3.558819905435939259E-15, 1.610000000000001874 ) ) ;
#9175=EDGE_LOOP ( 'NONE', ( #559, #1334, #10397 ) ) ;
#9186=ADVANCED_FACE ( 'NONE', ( #2273 ), #10103, .F. ) ;
#9195=LINE ( 'NONE', #9131, #11306 ) ;
#9200=( LENGTH_UNIT ( ) NAMED_UNIT ( * ) SI_UNIT ( .MILLI., .METRE. ) );
#9201=DIRECTION ( 'NONE',  ( 0.000000000000000000, 5.551115123125776539E-17, 1.000000000000000000 ) ) ;
#9208=LINE ( 'NONE', #4197, #11324 ) ;
#9213=CIRCLE ( 'NONE', #3682, 2.000000000000003109 ) ;
#9219=DIRECTION ( 'NONE',  ( 2.218671295934093250E-30, -5.551115123125776539E-17, -1.000000000000000000 ) ) ;
#9236=VECTOR ( 'NONE', #2920, 1000.000000000000114 ) ;
#9239=ORIENTED_EDGE ( 'NONE', *, *, #1522, .F. ) ;
#9244=CIRCLE ( 'NONE', #2277, 1.535500000000001863 ) ;
#9256=EDGE_CURVE ( 'NONE', #1582, #5079, #8376, .T. ) ;
#9258=ADVANCED_BREP_SHAPE_REPRESENTATION ( '', ( #10231, #12422 ), #7637 ) ;
#9295=ORIENTED_EDGE ( 'NONE', *, *, #4598, .F. ) ;
#9302=ORIENTED_EDGE ( 'NONE', *, *, #7782, .T. ) ;
#9325=AXIS2_PLACEMENT_3D ( 'NONE', #8999, #11133, #6236 ) ;
#9338=EDGE_CURVE ( 'NONE', #4187, #271, #11528, .T. ) ;
#9354=CARTESIAN_POINT ( 'NONE',  ( 0.000000000000000000, 1.773042676681338303, 0.000000000000000000 ) ) ;
#9374=DIRECTION ( 'NONE',  ( 7.038118388768703491E-30, 0.4999999999999988898, -0.8660254037844392627 ) ) ;
#9389=EDGE_LOOP ( 'NONE', ( #10512, #8860, #8283, #4084, #10080, #5826 ) ) ;
#9412=ADVANCED_FACE ( 'NONE', ( #1 ), #8878, .F. ) ;
#9425=VECTOR ( 'NONE', #2731, 1000.000000000000000 ) ;
#9428=ORIENTED_EDGE ( 'NONE', *, *, #6267, .T. ) ;
#9469=SURFACE_STYLE_USAGE ( .BOTH. , #8652 ) ;
#9472=VECTOR ( 'NONE', #2815, 1000.000000000000000 ) ;
#9480=ORIENTED_EDGE ( 'NONE', *, *, #10351, .T. ) ;
#9514=EDGE_CURVE ( 'NONE', #7720, #1057, #9636, .T. ) ;
#9524=CARTESIAN_POINT ( 'NONE',  ( 2.000000000000001776, 1.329782007511007169, -0.7677499999999976010 ) ) ;
#9533=SURFACE_STYLE_FILL_AREA ( #5565 ) ;
#9534=UNCERTAINTY_MEASURE_WITH_UNIT (LENGTH_MEASURE( 1.000000000000000082E-05 ), #1882, 'distance_accuracy_value', 'NONE');
#9535=DIRECTION ( 'NONE',  ( -1.000000000000000000, -1.031065855027150586E-29, 2.218671295934095703E-30 ) ) ;
#9543=DIRECTION ( 'NONE',  ( 1.000000000000000000, 1.031065855027150586E-29, -2.218671295934095703E-30 ) ) ;
#9574=CARTESIAN_POINT ( 'NONE',  ( 2.000000000000001776, 1.773042676681338303, 0.000000000000000000 ) ) ;
#9614=EDGE_CURVE ( 'NONE', #6684, #10144, #9195, .T. ) ;
#9615=ADVANCED_FACE ( 'NONE', ( #10022 ), #3907, .F. ) ;
#9633=EDGE_LOOP ( 'NONE', ( #8972, #7702, #5586, #2928, #9480 ) ) ;
#9636=CIRCLE ( 'NONE', #10675, 2.000000000000003109 ) ;
#9649=VECTOR ( 'NONE', #3874, 1000.000000000000000 ) ;
#9655=LINE ( 'NONE', #2002, #1588 ) ;
#9686=CARTESIAN_POINT ( 'NONE',  ( 28.99999999999999645, 3.469446951953614189E-15, 0.000000000000000000 ) ) ;
#9692=ORIENTED_EDGE ( 'NONE', *, *, #7001, .T. ) ;
#9700=DIRECTION ( 'NONE',  ( 0.000000000000000000, -5.551115123125775923E-17, -1.000000000000000000 ) ) ;
#9707=ORIENTED_EDGE ( 'NONE', *, *, #7362, .F. ) ;
#9729=CARTESIAN_POINT ( 'NONE',  ( 0.000000000000000000, -0.8865213383406727043, 1.535500000000009191 ) ) ;
#9734=CARTESIAN_POINT ( 'NONE',  ( -31.74999999999995026, 0.000000000000000000, 6.938893903907228378E-15 ) ) ;
#9742=EDGE_LOOP ( 'NONE', ( #4016, #8336 ) ) ;
#9743=CIRCLE ( 'NONE', #4238, 2.200000000000003730 ) ;
#9750=ORIENTED_EDGE ( 'NONE', *, *, #1500, .F. ) ;
#9771=DIRECTION ( 'NONE',  ( -0.7071067811865348052, 4.734329415644857690E-17, -0.7071067811865602293 ) ) ;
#9775=EDGE_CURVE ( 'NONE', #7469, #6684, #1471, .T. ) ;
#9781=AXIS2_PLACEMENT_3D ( 'NONE', #4013, #7933, #6199 ) ;
#9794=DIRECTION ( 'NONE',  ( 2.218671295934093250E-30, -5.551115123125776539E-17, -1.000000000000000000 ) ) ;
#9800=ORIENTED_EDGE ( 'NONE', *, *, #6369, .T. ) ;
#9818=ORIENTED_EDGE ( 'NONE', *, *, #658, .F. ) ;
#9834=ORIENTED_EDGE ( 'NONE', *, *, #6011, .T. ) ;
#9865=FACE_OUTER_BOUND ( 'NONE', #3099, .T. ) ;
#9867=VERTEX_POINT ( 'NONE', #5383 ) ;
#9910=CIRCLE ( 'NONE', #7674, 1.535500000000001863 ) ;
#9916=DIRECTION ( 'NONE',  ( -1.000000000000000000, -1.031065855027150586E-29, -2.218671295934092550E-30 ) ) ;
#9931=ORIENTED_EDGE ( 'NONE', *, *, #11450, .T. ) ;
#9933=SHAPE_DEFINITION_REPRESENTATION ( #11104, #4436 ) ;
#9966=CARTESIAN_POINT ( 'NONE',  ( 2.000000000000001776, 0.000000000000000000, 0.000000000000000000 ) ) ;
#9979=PLANE ( 'NONE',  #3981 ) ;
#10006=EDGE_LOOP ( 'NONE', ( #8934, #12530, #9818, #11367 ) ) ;
#10022=FACE_OUTER_BOUND ( 'NONE', #1668, .T. ) ;
#10035=DIRECTION ( 'NONE',  ( -1.000000000000000000, -1.031065855027150586E-29, 2.218671295934095703E-30 ) ) ;
#10047=DIRECTION ( 'NONE',  ( -2.218671295934095002E-30, -5.551115123125776539E-17, -1.000000000000000000 ) ) ;
#10063=DIRECTION ( 'NONE',  ( 0.000000000000000000, 5.551115123125777155E-17, 1.000000000000000000 ) ) ;
#10066=ADVANCED_FACE ( 'NONE', ( #9865 ), #7116, .T. ) ;
#10072=DIRECTION ( 'NONE',  ( -0.5000000000000056621, 5.798345671289627126E-17, -0.8660254037844352659 ) ) ;
#10080=ORIENTED_EDGE ( 'NONE', *, *, #8614, .F. ) ;
#10091=CARTESIAN_POINT ( 'NONE',  ( 0.000000000000000000, 0.8865213383406622683, -1.535499999999995202 ) ) ;
#10103=PLANE ( 'NONE',  #12334 ) ;
#10108=VERTEX_POINT ( 'NONE', #5892 ) ;
#10112=EDGE_CURVE ( 'NONE', #5079, #4568, #11824, .T. ) ;
#10118=EDGE_CURVE ( 'NONE', #10168, #2985, #3268, .T. ) ;
#10142=ORIENTED_EDGE ( 'NONE', *, *, #11605, .T. ) ;
#10144=VERTEX_POINT ( 'NONE', #1501 ) ;
#10148=DIRECTION ( 'NONE',  ( 1.000000000000000000, 1.031065855027150586E-29, -2.218671295934095703E-30 ) ) ;
#10168=VERTEX_POINT ( 'NONE', #2291 ) ;
#10179=DIRECTION ( 'NONE',  ( -2.218671295934095002E-30, -5.551115123125776539E-17, -1.000000000000000000 ) ) ;
#10216=PRESENTATION_STYLE_ASSIGNMENT (( #7226 ) ) ;
#10231=MANIFOLD_SOLID_BREP ( 'Hex', #4371 ) ;
#10254=CIRCLE ( 'NONE', #8626, 1.535500000000001863 ) ;
#10256=DIRECTION ( 'NONE',  ( 7.821394097150993714E-30, 0.8660254037844392627, 0.4999999999999991673 ) ) ;
#10270=EDGE_CURVE ( 'NONE', #6684, #4187, #10254, .T. ) ;
#10321=DIRECTION ( 'NONE',  ( -1.031065855027150586E-29, 1.000000000000000000, -1.779758311459930984E-16 ) ) ;
#10324=ORIENTED_EDGE ( 'NONE', *, *, #9338, .F. ) ;
#10339=DIRECTION ( 'NONE',  ( 1.000000000000000000, 1.031065855027150586E-29, -2.218671295934095703E-30 ) ) ;
#10340=DIRECTION ( 'NONE',  ( 0.000000000000000000, 5.551115123125777155E-17, 1.000000000000000000 ) ) ;
#10351=EDGE_CURVE ( 'NONE', #2985, #6306, #79, .T. ) ;
#10354=DIRECTION ( 'NONE',  ( 7.038118388768703491E-30, 0.4999999999999988898, -0.8660254037844392627 ) ) ;
#10378=DIRECTION ( 'NONE',  ( 7.038118388768703491E-30, 0.4999999999999988898, -0.8660254037844392627 ) ) ;
#10397=ORIENTED_EDGE ( 'NONE', *, *, #12352, .F. ) ;
#10398=FACE_OUTER_BOUND ( 'NONE', #9175, .T. ) ;
#10400=EDGE_LOOP ( 'NONE', ( #12555, #8290 ) ) ;
#10402=VERTEX_POINT ( 'NONE', #2998 ) ;
#10418=CIRCLE ( 'NONE', #1162, 0.2000000000000000944 ) ;
#10450=ORIENTED_EDGE ( 'NONE', *, *, #4338, .T. ) ;
#10463=ORIENTED_EDGE ( 'NONE', *, *, #11605, .F. ) ;
#10472=MECHANICAL_DESIGN_GEOMETRIC_PRESENTATION_REPRESENTATION('',(#12336),#5337);
#10512=ORIENTED_EDGE ( 'NONE', *, *, #4682, .T. ) ;
#10516=EDGE_CURVE ( 'NONE', #7272, #1057, #9208, .T. ) ;
#10529=ORIENTED_EDGE ( 'NONE', *, *, #342, .F. ) ;
#10550=LINE ( 'NONE', #12569, #2910 ) ;
#10572=( NAMED_UNIT ( * ) SI_UNIT ( $, .STERADIAN. ) SOLID_ANGLE_UNIT ( ) );
#10610=CARTESIAN_POINT ( 'NONE',  ( 2.000000000000001776, 0.000000000000000000, 0.000000000000000000 ) ) ;
#10631=CARTESIAN_POINT ( 'NONE',  ( 4.000000000000003553, 2.343373503925209768E-16, -3.500000000000000000 ) ) ;
#10647=FACE_OUTER_BOUND ( 'NONE', #12039, .T. ) ;
#10670=DIRECTION ( 'NONE',  ( 1.000000000000000000, 1.031065855027150586E-29, 2.218671295934092550E-30 ) ) ;
#10675=AXIS2_PLACEMENT_3D ( 'NONE', #12112, #10148, #7973 ) ;
#10677=CIRCLE ( 'NONE', #8833, 1.610000000000001874 ) ;
#10706=FACE_OUTER_BOUND ( 'NONE', #4586, .T. ) ;
#10721=DIRECTION ( 'NONE',  ( -3.260214209858707948E-30, -0.5000000000000012212, -0.8660254037844380415 ) ) ;
#10722=CARTESIAN_POINT ( 'NONE',  ( 2.000000000000001776, 1.773042676681338303, 0.000000000000000000 ) ) ;
#10723=VECTOR ( 'NONE', #7104, 1000.000000000000000 ) ;
#10760=EDGE_CURVE ( 'NONE', #11435, #7272, #3048, .T. ) ;
#10768=PLANE ( 'NONE',  #11026 ) ;
#10778=VERTEX_POINT ( 'NONE', #10810 ) ;
#10780=ORIENTED_EDGE ( 'NONE', *, *, #8084, .F. ) ;
#10810=CARTESIAN_POINT ( 'NONE',  ( 2.000000000000001776, -1.773042676681348739, 1.387778780781445676E-14 ) ) ;
#10814=VECTOR ( 'NONE', #7504, 1000.000000000000114 ) ;
#10831=CARTESIAN_POINT ( 'NONE',  ( 2.000000000000001776, 0.8865213383406622683, -1.535499999999995202 ) ) ;
#10847=ORIENTED_EDGE ( 'NONE', *, *, #4435, .T. ) ;
#10850=VERTEX_POINT ( 'NONE', #10091 ) ;
#10858=ORIENTED_EDGE ( 'NONE', *, *, #2018, .F. ) ;
#10884=CARTESIAN_POINT ( 'NONE',  ( 4.000000000000003553, 0.000000000000000000, 0.000000000000000000 ) ) ;
#10903=DIRECTION ( 'NONE',  ( -1.031065855027149465E-29, -1.000000000000000000, 7.771561172376086908E-16 ) ) ;
#10921=AXIS2_PLACEMENT_3D ( 'NONE', #12150, #1439, #9219 ) ;
#10927=ADVANCED_FACE ( 'NONE', ( #10398 ), #7222, .F. ) ;
#11003=CIRCLE ( 'NONE', #6276, 0.2000000000000000944 ) ;
#11016=DIRECTION ( 'NONE',  ( -1.000000000000000000, -1.031065855027150586E-29, 2.218671295934095703E-30 ) ) ;
#11026=AXIS2_PLACEMENT_3D ( 'NONE', #5696, #7759, #9794 ) ;
#11050=LINE ( 'NONE', #12218, #7792 ) ;
#11092=VECTOR ( 'NONE', #10378, 1000.000000000000114 ) ;
#11104=PRODUCT_DEFINITION_SHAPE ( 'NONE', 'NONE',  #4376 ) ;
#11133=DIRECTION ( 'NONE',  ( -1.000000000000000000, -1.031065855027150586E-29, 2.218671295934095703E-30 ) ) ;
#11146=SURFACE_STYLE_FILL_AREA ( #11210 ) ;
#11148=VECTOR ( 'NONE', #7919, 999.9999999999998863 ) ;
#11206=VERTEX_POINT ( 'NONE', #3962 ) ;
#11210=FILL_AREA_STYLE ('',( #7285 ) ) ;
#11220=AXIS2_PLACEMENT_3D ( 'NONE', #5513, #8404, #2698 ) ;
#11247=DIRECTION ( 'NONE',  ( -7.062770292056861511E-30, -0.4999999999999991673, 0.8660254037844392627 ) ) ;
#11248=VERTEX_POINT ( 'NONE', #7251 ) ;
#11250=LINE ( 'NONE', #7384, #5046 ) ;
#11264=DIRECTION ( 'NONE',  ( -1.000000000000000000, -1.031065855027150586E-29, 2.218671295934095703E-30 ) ) ;
#11280=ADVANCED_FACE ( 'NONE', ( #3578, #12404 ), #1373, .T. ) ;
#11290=CARTESIAN_POINT ( 'NONE',  ( 2.000000000000001776, 1.773042676681338303, 0.000000000000000000 ) ) ;
#11303=ORIENTED_EDGE ( 'NONE', *, *, #7003, .F. ) ;
#11306=VECTOR ( 'NONE', #1214, 1000.000000000000000 ) ;
#11308=FACE_OUTER_BOUND ( 'NONE', #1054, .T. ) ;
#11312=ORIENTED_EDGE ( 'NONE', *, *, #1676, .T. ) ;
#11324=VECTOR ( 'NONE', #4260, 1000.000000000000000 ) ;
#11328=ADVANCED_FACE ( 'NONE', ( #11432 ), #2510, .F. ) ;
#11342=( GEOMETRIC_REPRESENTATION_CONTEXT ( 3 ) GLOBAL_UNCERTAINTY_ASSIGNED_CONTEXT ( ( #12560 ) ) GLOBAL_UNIT_ASSIGNED_CONTEXT ( ( #7410, #2526, #1540 ) ) REPRESENTATION_CONTEXT ( 'NONE', 'WORKASPACE' ) );
#11367=ORIENTED_EDGE ( 'NONE', *, *, #6655, .F. ) ;
#11372=EDGE_CURVE ( 'NONE', #11435, #93, #2932, .T. ) ;
#11432=FACE_OUTER_BOUND ( 'NONE', #8233, .T. ) ;
#11435=VERTEX_POINT ( 'NONE', #12526 ) ;
#11450=EDGE_CURVE ( 'NONE', #1090, #7720, #1760, .T. ) ;
#11513=ORIENTED_EDGE ( 'NONE', *, *, #10351, .F. ) ;
#11527=LINE ( 'NONE', #11885, #11632 ) ;
#11528=CIRCLE ( 'NONE', #6588, 1.535500000000001863 ) ;
#11605=EDGE_CURVE ( 'NONE', #6292, #1053, #3000, .T. ) ;
#11611=DIRECTION ( 'NONE',  ( -3.260214209858707948E-30, -0.5000000000000012212, -0.8660254037844380415 ) ) ;
#11621=ORIENTED_EDGE ( 'NONE', *, *, #6655, .T. ) ;
#11622=CIRCLE ( 'NONE', #300, 0.2000000000000000944 ) ;
#11632=VECTOR ( 'NONE', #10903, 1000.000000000000000 ) ;
#11704=CARTESIAN_POINT ( 'NONE',  ( 2.000000000000001776, -0.8865213383406727043, 1.535500000000009191 ) ) ;
#11726=DIRECTION ( 'NONE',  ( -1.000000000000000000, -1.031065855027150586E-29, 2.218671295934095703E-30 ) ) ;
#11762=ORIENTED_EDGE ( 'NONE', *, *, #9256, .F. ) ;
#11777=DIRECTION ( 'NONE',  ( 0.000000000000000000, 5.551115123125777155E-17, 1.000000000000000000 ) ) ;
#11793=DIRECTION ( 'NONE',  ( 1.000000000000000000, 1.031065855027150586E-29, 2.218671295934092550E-30 ) ) ;
#11824=LINE ( 'NONE', #6330, #396 ) ;
#11826=EDGE_LOOP ( 'NONE', ( #4650, #11898, #11889, #9707 ) ) ;
#11839=DIRECTION ( 'NONE',  ( 1.000867273499157187E-29, 0.8660254037844380415, -0.5000000000000011102 ) ) ;
#11865=CARTESIAN_POINT ( 'NONE',  ( 0.000000000000000000, -0.8865213383406761460, -1.535499999999995202 ) ) ;
#11880=CARTESIAN_POINT ( 'NONE',  ( 0.000000000000000000, 1.773042676681338303, 0.000000000000000000 ) ) ;
#11885=CARTESIAN_POINT ( 'NONE',  ( 2.000000000000001776, 0.8865213383406622683, -1.535499999999995202 ) ) ;
#11889=ORIENTED_EDGE ( 'NONE', *, *, #7782, .F. ) ;
#11898=ORIENTED_EDGE ( 'NONE', *, *, #5869, .T. ) ;
#11911=ORIENTED_EDGE ( 'NONE', *, *, #4728, .T. ) ;
#11938=AXIS2_PLACEMENT_3D ( 'NONE', #5162, #7096, #9201 ) ;
#12039=EDGE_LOOP ( 'NONE', ( #6541, #10142, #8719, #7436 ) ) ;
#12044=ADVANCED_FACE ( 'NONE', ( #963 ), #192, .F. ) ;
#12051=CARTESIAN_POINT ( 'NONE',  ( 2.000000000000001776, 0.000000000000000000, 0.000000000000000000 ) ) ;
#12102=EDGE_LOOP ( 'NONE', ( #6372, #10450, #5734 ) ) ;
#12112=CARTESIAN_POINT ( 'NONE',  ( 4.200000000000001954, 0.000000000000000000, 0.000000000000000000 ) ) ;
#12150=CARTESIAN_POINT ( 'NONE',  ( 3.999999999999996447, 3.500000000000003109, 0.000000000000000000 ) ) ;
#12166=EDGE_LOOP ( 'NONE', ( #8087, #4475, #9295, #6703, #1844 ) ) ;
#12215=AXIS2_PLACEMENT_3D ( 'NONE', #10722, #1908, #5647 ) ;
#12218=CARTESIAN_POINT ( 'NONE',  ( 2.000000000000001776, -1.773042676681348739, 1.387778780781445676E-14 ) ) ;
#12220=LINE ( 'NONE', #3402, #1980 ) ;
#12222=DIRECTION ( 'NONE',  ( 0.000000000000000000, 5.551115123125776539E-17, 1.000000000000000000 ) ) ;
#12254=AXIS2_PLACEMENT_3D ( 'NONE', #9051, #2433, #8343 ) ;
#12270=DIRECTION ( 'NONE',  ( -3.260214209858707948E-30, -0.5000000000000012212, -0.8660254037844380415 ) ) ;
#12289=DIRECTION ( 'NONE',  ( 0.000000000000000000, -6.695352868347750602E-17, 1.000000000000000000 ) ) ;
#12328=DIRECTION ( 'NONE',  ( -1.000000000000000000, -1.031065855027150586E-29, 2.218671295934095703E-30 ) ) ;
#12334=AXIS2_PLACEMENT_3D ( 'NONE', #1291, #8049, #3187 ) ;
#12336=STYLED_ITEM ( 'NONE', ( #12403 ), #10231 ) ;
#12352=EDGE_CURVE ( 'NONE', #7997, #10168, #9910, .T. ) ;
#12403=PRESENTATION_STYLE_ASSIGNMENT (( #9469 ) ) ;
#12404=FACE_OUTER_BOUND ( 'NONE', #9742, .T. ) ;
#12422=AXIS2_PLACEMENT_3D ( 'NONE', #5707, #7392, #6428 ) ;
#12509=DIRECTION ( 'NONE',  ( -1.000000000000000000, -1.031065855027150586E-29, 2.218671295934095703E-30 ) ) ;
#12526=CARTESIAN_POINT ( 'NONE',  ( 28.99999999999999645, 3.590298071227288829E-15, -1.610000000000000098 ) ) ;
#12530=ORIENTED_EDGE ( 'NONE', *, *, #7003, .T. ) ;
#12534=CARTESIAN_POINT ( 'NONE',  ( 0.1999999999999987899, 0.000000000000000000, 0.000000000000000000 ) ) ;
#12555=ORIENTED_EDGE ( 'NONE', *, *, #658, .T. ) ;
#12560=UNCERTAINTY_MEASURE_WITH_UNIT (LENGTH_MEASURE( 1.000000000000000082E-05 ), #7410, 'distance_accuracy_value', 'NONE');
#12569=CARTESIAN_POINT ( 'NONE',  ( 0.000000000000000000, -1.773042676681359175, 1.387778780781445676E-14 ) ) ;
#12586=AXIS2_PLACEMENT_3D ( 'NONE', #6539, #474, #10179 ) ;
#12705=CIRCLE ( 'NONE', #800, 2.000000000000003553 ) ;
#12724=PLANE ( 'NONE',  #2623 ) ;
#12748=DIRECTION ( 'NONE',  ( -1.000000000000000000, -1.031065855027150586E-29, 2.218671295934095703E-30 ) ) ;
ENDSEC;
END-ISO-10303-21;
